ISO-10303-21;
HEADER;
/* Generated by software containing ST-Developer
 * from STEP Tools, Inc. (www.steptools.com) 
 */

FILE_DESCRIPTION(
/* description */ ('Rack and pinion manual slide'),
/* implementation_level */ '2;1');

FILE_NAME(
/* name */ 'Cap Screw - M4x16.step',
/* time_stamp */ '2026-10-28T03:22:49-07:00',
/* author */ (''),
/* organization */ (''),
/* preprocessor_version */ 'ST-DEVELOPER v20.2',
/* originating_system */ 'Autodesk Translation Framework v15.17.0.0',
/* authorisation */ '');

FILE_SCHEMA (('AUTOMOTIVE_DESIGN { 1 0 10303 214 3 1 1 }'));
ENDSEC;

DATA;
#10=MECHANICAL_DESIGN_GEOMETRIC_PRESENTATION_REPRESENTATION('',(#780),#34851);
#608=ORIENTED_CLOSED_SHELL('',*,#13804,.F.);
#613=BREP_WITH_VOIDS('Body1',#13803,(#608));
#630=CONICAL_SURFACE('',#15418,0.325,0.785398163397448);
#631=CONICAL_SURFACE('',#15422,0.335,0.785398163397448);
#632=CONICAL_SURFACE('',#15426,0.21,0.463647609000806);
#633=CONICAL_SURFACE('',#15430,0.18,0.785398163397448);
#681=SHAPE_REPRESENTATION_RELATIONSHIP('SRR','None',#35120,#727);
#727=ADVANCED_BREP_SHAPE_REPRESENTATION('',(#613),#34845);
#780=STYLED_ITEM('',(#35418),#613);
#1038=FACE_BOUND('',#3171,.T.);
#1499=PLANE('',#15416);
#1500=PLANE('',#15424);
#1501=PLANE('',#15432);
#1502=PLANE('',#15433);
#1503=PLANE('',#15434);
#1504=PLANE('',#15435);
#1505=PLANE('',#15436);
#1506=PLANE('',#15437);
#1507=PLANE('',#15438);
#1508=PLANE('',#15439);
#1509=PLANE('',#15440);
#2222=FACE_OUTER_BOUND('',#3166,.T.);
#2223=FACE_OUTER_BOUND('',#3167,.T.);
#2224=FACE_OUTER_BOUND('',#3168,.T.);
#2225=FACE_OUTER_BOUND('',#3169,.T.);
#2226=FACE_OUTER_BOUND('',#3170,.T.);
#2227=FACE_OUTER_BOUND('',#3172,.T.);
#2228=FACE_OUTER_BOUND('',#3173,.T.);
#2229=FACE_OUTER_BOUND('',#3174,.T.);
#2230=FACE_OUTER_BOUND('',#3175,.T.);
#2231=FACE_OUTER_BOUND('',#3176,.T.);
#2232=FACE_OUTER_BOUND('',#3177,.T.);
#2233=FACE_OUTER_BOUND('',#3178,.T.);
#2234=FACE_OUTER_BOUND('',#3179,.T.);
#2235=FACE_OUTER_BOUND('',#3180,.T.);
#2236=FACE_OUTER_BOUND('',#3181,.T.);
#2237=FACE_OUTER_BOUND('',#3182,.T.);
#2238=FACE_OUTER_BOUND('',#3183,.T.);
#3166=EDGE_LOOP('',(#12644));
#3167=EDGE_LOOP('',(#12645,#12646,#12647,#12648));
#3168=EDGE_LOOP('',(#12649,#12650,#12651,#12652));
#3169=EDGE_LOOP('',(#12653,#12654,#12655,#12656));
#3170=EDGE_LOOP('',(#12657));
#3171=EDGE_LOOP('',(#12658));
#3172=EDGE_LOOP('',(#12659,#12660,#12661,#12662));
#3173=EDGE_LOOP('',(#12663,#12664,#12665,#12666));
#3174=EDGE_LOOP('',(#12667,#12668,#12669,#12670));
#3175=EDGE_LOOP('',(#12671));
#3176=EDGE_LOOP('',(#12672,#12673,#12674,#12675));
#3177=EDGE_LOOP('',(#12676,#12677,#12678,#12679));
#3178=EDGE_LOOP('',(#12680,#12681,#12682,#12683));
#3179=EDGE_LOOP('',(#12684,#12685,#12686,#12687));
#3180=EDGE_LOOP('',(#12688,#12689,#12690,#12691));
#3181=EDGE_LOOP('',(#12692,#12693,#12694,#12695));
#3182=EDGE_LOOP('',(#12696,#12697,#12698,#12699,#12700,#12701));
#3183=EDGE_LOOP('',(#12702,#12703,#12704,#12705,#12706,#12707));
#4439=LINE('',#34426,#5730);
#4440=LINE('',#34430,#5731);
#4441=LINE('',#34434,#5732);
#4442=LINE('',#34441,#5733);
#4443=LINE('',#34445,#5734);
#4444=LINE('',#34449,#5735);
#4445=LINE('',#34454,#5736);
#4446=LINE('',#34456,#5737);
#4447=LINE('',#34458,#5738);
#4448=LINE('',#34459,#5739);
#4449=LINE('',#34462,#5740);
#4450=LINE('',#34464,#5741);
#4451=LINE('',#34465,#5742);
#4452=LINE('',#34468,#5743);
#4453=LINE('',#34470,#5744);
#4454=LINE('',#34471,#5745);
#4455=LINE('',#34474,#5746);
#4456=LINE('',#34476,#5747);
#4457=LINE('',#34477,#5748);
#4458=LINE('',#34480,#5749);
#4459=LINE('',#34482,#5750);
#4460=LINE('',#34483,#5751);
#4461=LINE('',#34485,#5752);
#4462=LINE('',#34486,#5753);
#5730=VECTOR('',#19021,0.325);
#5731=VECTOR('',#19026,0.35);
#5732=VECTOR('',#19031,0.335);
#5733=VECTOR('',#19040,0.21);
#5734=VECTOR('',#19045,0.2);
#5735=VECTOR('',#19050,0.18);
#5736=VECTOR('',#19055,1.);
#5737=VECTOR('',#19056,1.);
#5738=VECTOR('',#19057,1.);
#5739=VECTOR('',#19058,1.);
#5740=VECTOR('',#19061,1.);
#5741=VECTOR('',#19062,1.);
#5742=VECTOR('',#19063,1.);
#5743=VECTOR('',#19066,1.);
#5744=VECTOR('',#19067,1.);
#5745=VECTOR('',#19068,1.);
#5746=VECTOR('',#19071,1.);
#5747=VECTOR('',#19072,1.);
#5748=VECTOR('',#19073,1.);
#5749=VECTOR('',#19076,1.);
#5750=VECTOR('',#19077,1.);
#5751=VECTOR('',#19078,1.);
#5752=VECTOR('',#19081,1.);
#5753=VECTOR('',#19082,1.);
#6200=CIRCLE('',#15417,0.3);
#6201=CIRCLE('',#15419,0.35);
#6202=CIRCLE('',#15421,0.35);
#6203=CIRCLE('',#15423,0.32);
#6204=CIRCLE('',#15425,0.22);
#6205=CIRCLE('',#15427,0.1954);
#6206=CIRCLE('',#15429,0.1954);
#6207=CIRCLE('',#15431,0.16);
#7365=VERTEX_POINT('',#34421);
#7366=VERTEX_POINT('',#34424);
#7367=VERTEX_POINT('',#34428);
#7368=VERTEX_POINT('',#34432);
#7369=VERTEX_POINT('',#34436);
#7370=VERTEX_POINT('',#34439);
#7371=VERTEX_POINT('',#34443);
#7372=VERTEX_POINT('',#34447);
#7373=VERTEX_POINT('',#34452);
#7374=VERTEX_POINT('',#34453);
#7375=VERTEX_POINT('',#34455);
#7376=VERTEX_POINT('',#34457);
#7377=VERTEX_POINT('',#34461);
#7378=VERTEX_POINT('',#34463);
#7379=VERTEX_POINT('',#34467);
#7380=VERTEX_POINT('',#34469);
#7381=VERTEX_POINT('',#34473);
#7382=VERTEX_POINT('',#34475);
#7383=VERTEX_POINT('',#34479);
#7384=VERTEX_POINT('',#34481);
#9134=EDGE_CURVE('',#7365,#7365,#6200,.T.);
#9135=EDGE_CURVE('',#7366,#7366,#6201,.T.);
#9136=EDGE_CURVE('',#7366,#7365,#4439,.T.);
#9137=EDGE_CURVE('',#7367,#7367,#6202,.T.);
#9138=EDGE_CURVE('',#7367,#7366,#4440,.T.);
#9139=EDGE_CURVE('',#7368,#7368,#6203,.T.);
#9140=EDGE_CURVE('',#7368,#7367,#4441,.T.);
#9141=EDGE_CURVE('',#7369,#7369,#6204,.T.);
#9142=EDGE_CURVE('',#7370,#7370,#6205,.F.);
#9143=EDGE_CURVE('',#7370,#7369,#4442,.T.);
#9144=EDGE_CURVE('',#7371,#7371,#6206,.F.);
#9145=EDGE_CURVE('',#7371,#7370,#4443,.T.);
#9146=EDGE_CURVE('',#7372,#7372,#6207,.T.);
#9147=EDGE_CURVE('',#7372,#7371,#4444,.T.);
#9148=EDGE_CURVE('',#7373,#7374,#4445,.T.);
#9149=EDGE_CURVE('',#7374,#7375,#4446,.T.);
#9150=EDGE_CURVE('',#7375,#7376,#4447,.T.);
#9151=EDGE_CURVE('',#7373,#7376,#4448,.T.);
#9152=EDGE_CURVE('',#7374,#7377,#4449,.T.);
#9153=EDGE_CURVE('',#7377,#7378,#4450,.T.);
#9154=EDGE_CURVE('',#7378,#7375,#4451,.T.);
#9155=EDGE_CURVE('',#7377,#7379,#4452,.T.);
#9156=EDGE_CURVE('',#7379,#7380,#4453,.T.);
#9157=EDGE_CURVE('',#7380,#7378,#4454,.T.);
#9158=EDGE_CURVE('',#7379,#7381,#4455,.T.);
#9159=EDGE_CURVE('',#7381,#7382,#4456,.T.);
#9160=EDGE_CURVE('',#7382,#7380,#4457,.T.);
#9161=EDGE_CURVE('',#7381,#7383,#4458,.T.);
#9162=EDGE_CURVE('',#7383,#7384,#4459,.T.);
#9163=EDGE_CURVE('',#7384,#7382,#4460,.T.);
#9164=EDGE_CURVE('',#7383,#7373,#4461,.T.);
#9165=EDGE_CURVE('',#7376,#7384,#4462,.T.);
#12644=ORIENTED_EDGE('',*,*,#9134,.F.);
#12645=ORIENTED_EDGE('',*,*,#9135,.F.);
#12646=ORIENTED_EDGE('',*,*,#9136,.T.);
#12647=ORIENTED_EDGE('',*,*,#9134,.T.);
#12648=ORIENTED_EDGE('',*,*,#9136,.F.);
#12649=ORIENTED_EDGE('',*,*,#9137,.F.);
#12650=ORIENTED_EDGE('',*,*,#9138,.T.);
#12651=ORIENTED_EDGE('',*,*,#9135,.T.);
#12652=ORIENTED_EDGE('',*,*,#9138,.F.);
#12653=ORIENTED_EDGE('',*,*,#9139,.F.);
#12654=ORIENTED_EDGE('',*,*,#9140,.T.);
#12655=ORIENTED_EDGE('',*,*,#9137,.T.);
#12656=ORIENTED_EDGE('',*,*,#9140,.F.);
#12657=ORIENTED_EDGE('',*,*,#9139,.T.);
#12658=ORIENTED_EDGE('',*,*,#9141,.F.);
#12659=ORIENTED_EDGE('',*,*,#9142,.F.);
#12660=ORIENTED_EDGE('',*,*,#9143,.T.);
#12661=ORIENTED_EDGE('',*,*,#9141,.T.);
#12662=ORIENTED_EDGE('',*,*,#9143,.F.);
#12663=ORIENTED_EDGE('',*,*,#9144,.F.);
#12664=ORIENTED_EDGE('',*,*,#9145,.T.);
#12665=ORIENTED_EDGE('',*,*,#9142,.T.);
#12666=ORIENTED_EDGE('',*,*,#9145,.F.);
#12667=ORIENTED_EDGE('',*,*,#9146,.F.);
#12668=ORIENTED_EDGE('',*,*,#9147,.T.);
#12669=ORIENTED_EDGE('',*,*,#9144,.T.);
#12670=ORIENTED_EDGE('',*,*,#9147,.F.);
#12671=ORIENTED_EDGE('',*,*,#9146,.T.);
#12672=ORIENTED_EDGE('',*,*,#9148,.T.);
#12673=ORIENTED_EDGE('',*,*,#9149,.T.);
#12674=ORIENTED_EDGE('',*,*,#9150,.T.);
#12675=ORIENTED_EDGE('',*,*,#9151,.F.);
#12676=ORIENTED_EDGE('',*,*,#9152,.T.);
#12677=ORIENTED_EDGE('',*,*,#9153,.T.);
#12678=ORIENTED_EDGE('',*,*,#9154,.T.);
#12679=ORIENTED_EDGE('',*,*,#9149,.F.);
#12680=ORIENTED_EDGE('',*,*,#9155,.T.);
#12681=ORIENTED_EDGE('',*,*,#9156,.T.);
#12682=ORIENTED_EDGE('',*,*,#9157,.T.);
#12683=ORIENTED_EDGE('',*,*,#9153,.F.);
#12684=ORIENTED_EDGE('',*,*,#9158,.T.);
#12685=ORIENTED_EDGE('',*,*,#9159,.T.);
#12686=ORIENTED_EDGE('',*,*,#9160,.T.);
#12687=ORIENTED_EDGE('',*,*,#9156,.F.);
#12688=ORIENTED_EDGE('',*,*,#9161,.T.);
#12689=ORIENTED_EDGE('',*,*,#9162,.T.);
#12690=ORIENTED_EDGE('',*,*,#9163,.T.);
#12691=ORIENTED_EDGE('',*,*,#9159,.F.);
#12692=ORIENTED_EDGE('',*,*,#9164,.T.);
#12693=ORIENTED_EDGE('',*,*,#9151,.T.);
#12694=ORIENTED_EDGE('',*,*,#9165,.T.);
#12695=ORIENTED_EDGE('',*,*,#9162,.F.);
#12696=ORIENTED_EDGE('',*,*,#9164,.F.);
#12697=ORIENTED_EDGE('',*,*,#9161,.F.);
#12698=ORIENTED_EDGE('',*,*,#9158,.F.);
#12699=ORIENTED_EDGE('',*,*,#9155,.F.);
#12700=ORIENTED_EDGE('',*,*,#9152,.F.);
#12701=ORIENTED_EDGE('',*,*,#9148,.F.);
#12702=ORIENTED_EDGE('',*,*,#9165,.F.);
#12703=ORIENTED_EDGE('',*,*,#9150,.F.);
#12704=ORIENTED_EDGE('',*,*,#9154,.F.);
#12705=ORIENTED_EDGE('',*,*,#9157,.F.);
#12706=ORIENTED_EDGE('',*,*,#9160,.F.);
#12707=ORIENTED_EDGE('',*,*,#9163,.F.);
#13005=CYLINDRICAL_SURFACE('',#15420,0.35);
#13006=CYLINDRICAL_SURFACE('',#15428,0.1954);
#13700=ADVANCED_FACE('',(#2222),#1499,.T.);
#13701=ADVANCED_FACE('',(#2223),#630,.T.);
#13702=ADVANCED_FACE('',(#2224),#13005,.T.);
#13703=ADVANCED_FACE('',(#2225),#631,.T.);
#13704=ADVANCED_FACE('',(#2226,#1038),#1500,.T.);
#13705=ADVANCED_FACE('',(#2227),#632,.T.);
#13706=ADVANCED_FACE('',(#2228),#13006,.T.);
#13707=ADVANCED_FACE('',(#2229),#633,.T.);
#13708=ADVANCED_FACE('',(#2230),#1501,.T.);
#13709=ADVANCED_FACE('',(#2231),#1502,.F.);
#13710=ADVANCED_FACE('',(#2232),#1503,.F.);
#13711=ADVANCED_FACE('',(#2233),#1504,.F.);
#13712=ADVANCED_FACE('',(#2234),#1505,.F.);
#13713=ADVANCED_FACE('',(#2235),#1506,.F.);
#13714=ADVANCED_FACE('',(#2236),#1507,.F.);
#13715=ADVANCED_FACE('',(#2237),#1508,.F.);
#13716=ADVANCED_FACE('',(#2238),#1509,.F.);
#13803=CLOSED_SHELL('',(#13700,#13701,#13702,#13703,#13704,#13705,#13706,
#13707,#13708));
#13804=CLOSED_SHELL('',(#13709,#13710,#13711,#13712,#13713,#13714,#13715,
#13716));
#15415=AXIS2_PLACEMENT_3D('',#34419,#19011,#19012);
#15416=AXIS2_PLACEMENT_3D('',#34420,#19013,#19014);
#15417=AXIS2_PLACEMENT_3D('',#34422,#19015,#19016);
#15418=AXIS2_PLACEMENT_3D('',#34423,#19017,#19018);
#15419=AXIS2_PLACEMENT_3D('',#34425,#19019,#19020);
#15420=AXIS2_PLACEMENT_3D('',#34427,#19022,#19023);
#15421=AXIS2_PLACEMENT_3D('',#34429,#19024,#19025);
#15422=AXIS2_PLACEMENT_3D('',#34431,#19027,#19028);
#15423=AXIS2_PLACEMENT_3D('',#34433,#19029,#19030);
#15424=AXIS2_PLACEMENT_3D('',#34435,#19032,#19033);
#15425=AXIS2_PLACEMENT_3D('',#34437,#19034,#19035);
#15426=AXIS2_PLACEMENT_3D('',#34438,#19036,#19037);
#15427=AXIS2_PLACEMENT_3D('',#34440,#19038,#19039);
#15428=AXIS2_PLACEMENT_3D('',#34442,#19041,#19042);
#15429=AXIS2_PLACEMENT_3D('',#34444,#19043,#19044);
#15430=AXIS2_PLACEMENT_3D('',#34446,#19046,#19047);
#15431=AXIS2_PLACEMENT_3D('',#34448,#19048,#19049);
#15432=AXIS2_PLACEMENT_3D('',#34450,#19051,#19052);
#15433=AXIS2_PLACEMENT_3D('',#34451,#19053,#19054);
#15434=AXIS2_PLACEMENT_3D('',#34460,#19059,#19060);
#15435=AXIS2_PLACEMENT_3D('',#34466,#19064,#19065);
#15436=AXIS2_PLACEMENT_3D('',#34472,#19069,#19070);
#15437=AXIS2_PLACEMENT_3D('',#34478,#19074,#19075);
#15438=AXIS2_PLACEMENT_3D('',#34484,#19079,#19080);
#15439=AXIS2_PLACEMENT_3D('',#34487,#19083,#19084);
#15440=AXIS2_PLACEMENT_3D('',#34488,#19085,#19086);
#19011=DIRECTION('axis',(0.,0.,1.));
#19012=DIRECTION('refdir',(1.,0.,0.));
#19013=DIRECTION('center_axis',(0.,1.,0.));
#19014=DIRECTION('ref_axis',(0.,0.,1.));
#19015=DIRECTION('center_axis',(0.,-1.,0.));
#19016=DIRECTION('ref_axis',(1.,0.,0.));
#19017=DIRECTION('center_axis',(0.,-1.,0.));
#19018=DIRECTION('ref_axis',(1.,0.,0.));
#19019=DIRECTION('center_axis',(0.,-1.,0.));
#19020=DIRECTION('ref_axis',(1.,0.,0.));
#19021=DIRECTION('',(0.707106781186547,0.707106781186548,8.65956056235493E-17));
#19022=DIRECTION('center_axis',(0.,-1.,0.));
#19023=DIRECTION('ref_axis',(1.,0.,0.));
#19024=DIRECTION('center_axis',(0.,-1.,0.));
#19025=DIRECTION('ref_axis',(1.,0.,0.));
#19026=DIRECTION('',(0.,1.,0.));
#19027=DIRECTION('center_axis',(0.,1.,0.));
#19028=DIRECTION('ref_axis',(1.,0.,0.));
#19029=DIRECTION('center_axis',(0.,-1.,0.));
#19030=DIRECTION('ref_axis',(1.,0.,0.));
#19031=DIRECTION('',(-0.707106781186547,0.707106781186548,-8.65956056235493E-17));
#19032=DIRECTION('center_axis',(0.,-1.,0.));
#19033=DIRECTION('ref_axis',(0.,0.,-1.));
#19034=DIRECTION('center_axis',(0.,-1.,0.));
#19035=DIRECTION('ref_axis',(1.,0.,0.));
#19036=DIRECTION('center_axis',(0.,1.,0.));
#19037=DIRECTION('ref_axis',(1.,0.,0.));
#19038=DIRECTION('center_axis',(0.,1.,0.));
#19039=DIRECTION('ref_axis',(1.,0.,0.));
#19040=DIRECTION('',(-0.447213595499958,0.894427190999916,-5.47678698264203E-17));
#19041=DIRECTION('center_axis',(0.,-1.,0.));
#19042=DIRECTION('ref_axis',(1.,0.,0.));
#19043=DIRECTION('center_axis',(0.,1.,0.));
#19044=DIRECTION('ref_axis',(1.,0.,0.));
#19045=DIRECTION('',(0.,1.,0.));
#19046=DIRECTION('center_axis',(0.,1.,0.));
#19047=DIRECTION('ref_axis',(1.,0.,0.));
#19048=DIRECTION('center_axis',(0.,-1.,0.));
#19049=DIRECTION('ref_axis',(1.,0.,0.));
#19050=DIRECTION('',(-0.707106781186547,0.707106781186548,-8.65956056235493E-17));
#19051=DIRECTION('center_axis',(0.,-1.,0.));
#19052=DIRECTION('ref_axis',(0.,0.,-1.));
#19053=DIRECTION('center_axis',(0.866025403784439,0.,-0.5));
#19054=DIRECTION('ref_axis',(0.5,0.,0.866025403784439));
#19055=DIRECTION('',(-0.5,0.,-0.866025403784439));
#19056=DIRECTION('',(0.,-1.,0.));
#19057=DIRECTION('',(0.5,0.,0.866025403784439));
#19058=DIRECTION('',(0.,-1.,0.));
#19059=DIRECTION('center_axis',(1.60246890531964E-16,0.,-1.));
#19060=DIRECTION('ref_axis',(1.,0.,1.60246890531964E-16));
#19061=DIRECTION('',(-1.,0.,-1.60246890531964E-16));
#19062=DIRECTION('',(0.,-1.,0.));
#19063=DIRECTION('',(1.,0.,1.60246890531964E-16));
#19064=DIRECTION('center_axis',(-0.866025403784439,0.,-0.5));
#19065=DIRECTION('ref_axis',(0.5,0.,-0.866025403784439));
#19066=DIRECTION('',(-0.5,0.,0.866025403784439));
#19067=DIRECTION('',(0.,-1.,0.));
#19068=DIRECTION('',(0.5,0.,-0.866025403784439));
#19069=DIRECTION('center_axis',(-0.866025403784439,0.,0.5));
#19070=DIRECTION('ref_axis',(-0.5,0.,-0.866025403784439));
#19071=DIRECTION('',(0.5,0.,0.866025403784439));
#19072=DIRECTION('',(0.,-1.,0.));
#19073=DIRECTION('',(-0.5,0.,-0.866025403784439));
#19074=DIRECTION('center_axis',(-1.60246890531964E-16,0.,1.));
#19075=DIRECTION('ref_axis',(-1.,0.,-1.60246890531964E-16));
#19076=DIRECTION('',(1.,0.,1.60246890531964E-16));
#19077=DIRECTION('',(0.,-1.,0.));
#19078=DIRECTION('',(-1.,0.,-1.60246890531964E-16));
#19079=DIRECTION('center_axis',(0.866025403784439,0.,0.5));
#19080=DIRECTION('ref_axis',(-0.5,0.,0.866025403784439));
#19081=DIRECTION('',(0.5,0.,-0.866025403784439));
#19082=DIRECTION('',(-0.5,0.,0.866025403784439));
#19083=DIRECTION('center_axis',(0.,1.,0.));
#19084=DIRECTION('ref_axis',(1.,0.,0.));
#19085=DIRECTION('center_axis',(0.,-1.,0.));
#19086=DIRECTION('ref_axis',(0.,0.,-1.));
#34419=CARTESIAN_POINT('',(0.,0.,0.));
#34420=CARTESIAN_POINT('Origin',(0.3,0.4,0.));
#34421=CARTESIAN_POINT('',(-0.3,0.4,-3.67394039744206E-17));
#34422=CARTESIAN_POINT('Origin',(0.,0.4,0.));
#34423=CARTESIAN_POINT('Origin',(0.,0.375,0.));
#34424=CARTESIAN_POINT('',(-0.35,0.35,-4.28626379701573E-17));
#34425=CARTESIAN_POINT('Origin',(0.,0.35,0.));
#34426=CARTESIAN_POINT('',(-0.325,0.375,-3.9801020972289E-17));
#34427=CARTESIAN_POINT('Origin',(0.,0.19,0.));
#34428=CARTESIAN_POINT('',(-0.35,0.03,-4.28626379701574E-17));
#34429=CARTESIAN_POINT('Origin',(0.,0.03,0.));
#34430=CARTESIAN_POINT('',(-0.35,0.19,-4.28626379701574E-17));
#34431=CARTESIAN_POINT('Origin',(0.,0.0149999999999999,0.));
#34432=CARTESIAN_POINT('',(-0.32,-3.29597460435593E-17,-3.91886975727153E-17));
#34433=CARTESIAN_POINT('Origin',(0.,0.,0.));
#34434=CARTESIAN_POINT('',(-0.335,0.0149999999999999,-4.10256677714363E-17));
#34435=CARTESIAN_POINT('Origin',(0.22,0.,0.));
#34436=CARTESIAN_POINT('',(-0.22,-6.93889390390723E-18,-2.69422295812418E-17));
#34437=CARTESIAN_POINT('Origin',(0.,0.,0.));
#34438=CARTESIAN_POINT('Origin',(0.,-0.02,0.));
#34439=CARTESIAN_POINT('',(-0.1954,-0.0492,2.39295984553393E-17));
#34440=CARTESIAN_POINT('Origin',(0.,-0.0492,0.));
#34441=CARTESIAN_POINT('',(-0.21,-0.02,-2.57175827820944E-17));
#34442=CARTESIAN_POINT('Origin',(0.,-0.8,0.));
#34443=CARTESIAN_POINT('',(-0.1954,-1.5646,2.39295984553393E-17));
#34444=CARTESIAN_POINT('Origin',(0.,-1.5646,0.));
#34445=CARTESIAN_POINT('',(-0.1954,-0.8,-2.39295984553393E-17));
#34446=CARTESIAN_POINT('Origin',(0.,-1.58,0.));
#34447=CARTESIAN_POINT('',(-0.16,-1.6,-1.95943487863577E-17));
#34448=CARTESIAN_POINT('Origin',(0.,-1.6,0.));
#34449=CARTESIAN_POINT('',(-0.18,-1.58,-2.20436423846524E-17));
#34450=CARTESIAN_POINT('Origin',(0.,-1.6,0.));
#34451=CARTESIAN_POINT('Origin',(0.0866025403784439,-0.4,-0.15));
#34452=CARTESIAN_POINT('',(0.173205080756888,-0.4,0.));
#34453=CARTESIAN_POINT('',(0.0866025403784439,-0.4,-0.15));
#34454=CARTESIAN_POINT('',(0.173205080756888,-0.4,0.));
#34455=CARTESIAN_POINT('',(0.0866025403784439,-0.64,-0.15));
#34456=CARTESIAN_POINT('',(0.0866025403784439,-0.4,-0.15));
#34457=CARTESIAN_POINT('',(0.173205080756888,-0.64,0.));
#34458=CARTESIAN_POINT('',(0.173205080756888,-0.64,0.));
#34459=CARTESIAN_POINT('',(0.173205080756888,-0.4,0.));
#34460=CARTESIAN_POINT('Origin',(-0.0866025403784438,-0.4,-0.15));
#34461=CARTESIAN_POINT('',(-0.0866025403784438,-0.4,-0.15));
#34462=CARTESIAN_POINT('',(0.0866025403784439,-0.4,-0.15));
#34463=CARTESIAN_POINT('',(-0.0866025403784438,-0.64,-0.15));
#34464=CARTESIAN_POINT('',(-0.0866025403784438,-0.4,-0.15));
#34465=CARTESIAN_POINT('',(0.0866025403784439,-0.64,-0.15));
#34466=CARTESIAN_POINT('Origin',(-0.173205080756888,-0.4,-2.77555756156289E-17));
#34467=CARTESIAN_POINT('',(-0.173205080756888,-0.4,-2.12115047744981E-17));
#34468=CARTESIAN_POINT('',(-0.0866025403784438,-0.4,-0.15));
#34469=CARTESIAN_POINT('',(-0.173205080756888,-0.64,-2.77555756156289E-17));
#34470=CARTESIAN_POINT('',(-0.173205080756888,-0.4,-2.12115047744981E-17));
#34471=CARTESIAN_POINT('',(-0.0866025403784438,-0.64,-0.15));
#34472=CARTESIAN_POINT('Origin',(-0.0866025403784439,-0.4,0.15));
#34473=CARTESIAN_POINT('',(-0.0866025403784439,-0.4,0.15));
#34474=CARTESIAN_POINT('',(-0.173205080756888,-0.4,-2.12115047744981E-17));
#34475=CARTESIAN_POINT('',(-0.0866025403784439,-0.64,0.15));
#34476=CARTESIAN_POINT('',(-0.0866025403784439,-0.4,0.15));
#34477=CARTESIAN_POINT('',(-0.173205080756888,-0.64,-2.12115047744981E-17));
#34478=CARTESIAN_POINT('Origin',(0.0866025403784439,-0.4,0.15));
#34479=CARTESIAN_POINT('',(0.0866025403784439,-0.4,0.15));
#34480=CARTESIAN_POINT('',(-0.0866025403784439,-0.4,0.15));
#34481=CARTESIAN_POINT('',(0.0866025403784439,-0.64,0.15));
#34482=CARTESIAN_POINT('',(0.0866025403784439,-0.4,0.15));
#34483=CARTESIAN_POINT('',(-0.0866025403784439,-0.64,0.15));
#34484=CARTESIAN_POINT('Origin',(0.173205080756888,-0.4,0.));
#34485=CARTESIAN_POINT('',(0.0866025403784439,-0.4,0.15));
#34486=CARTESIAN_POINT('',(0.0866025403784439,-0.64,0.15));
#34487=CARTESIAN_POINT('Origin',(0.,-0.4,-2.77555756156289E-17));
#34488=CARTESIAN_POINT('Origin',(0.,-0.64,-2.77555756156289E-17));
#34791=UNCERTAINTY_MEASURE_WITH_UNIT(LENGTH_MEASURE(0.001),#34852,
'DISTANCE_ACCURACY_VALUE',
'Maximum model space distance between geometric entities at asserted c
onnectivities');
#34797=UNCERTAINTY_MEASURE_WITH_UNIT(LENGTH_MEASURE(0.001),#34852,
'DISTANCE_ACCURACY_VALUE',
'Maximum model space distance between geometric entities at asserted c
onnectivities');
#34845=(
GEOMETRIC_REPRESENTATION_CONTEXT(3)
GLOBAL_UNCERTAINTY_ASSIGNED_CONTEXT((#34791))
GLOBAL_UNIT_ASSIGNED_CONTEXT((#34852,#34854,#34855))
REPRESENTATION_CONTEXT('','3D')
);
#34851=(
GEOMETRIC_REPRESENTATION_CONTEXT(3)
GLOBAL_UNCERTAINTY_ASSIGNED_CONTEXT((#34797))
GLOBAL_UNIT_ASSIGNED_CONTEXT((#34852,#34854,#34855))
REPRESENTATION_CONTEXT('','3D')
);
#34852=(
LENGTH_UNIT()
NAMED_UNIT(*)
SI_UNIT(.CENTI.,.METRE.)
);
#34854=(
NAMED_UNIT(*)
PLANE_ANGLE_UNIT()
SI_UNIT($,.RADIAN.)
);
#34855=(
NAMED_UNIT(*)
SI_UNIT($,.STERADIAN.)
SOLID_ANGLE_UNIT()
);
#34903=SHAPE_DEFINITION_REPRESENTATION(#34964,#35120);
#34964=PRODUCT_DEFINITION_SHAPE('',$,#35174);
#35120=SHAPE_REPRESENTATION('',(#15415),#34845);
#35126=PRODUCT_DEFINITION_CONTEXT('part definition',#35287,'design');
#35174=PRODUCT_DEFINITION('Cap Screw - M4x16','Cap Screw - M4x16',#35227,
#35126);
#35227=PRODUCT_DEFINITION_FORMATION('',$,#35336);
#35287=APPLICATION_CONTEXT(
'Core Data for Automotive Mechanical Design Process');
#35288=PRODUCT_CONTEXT('part definition',#35287,'mechanical');
#35336=PRODUCT('Cap Screw - M4x16','Cap Screw - M4x16',
'Cap Screw - M4x16',(#35288));
#35412=COLOUR_RGB('Black',0.12,0.14,0.17);
#35413=FILL_AREA_STYLE_COLOUR('',#35412);
#35414=FILL_AREA_STYLE('',(#35413));
#35415=SURFACE_STYLE_FILL_AREA(#35414);
#35416=SURFACE_SIDE_STYLE('',(#35415));
#35417=SURFACE_STYLE_USAGE(.BOTH.,#35416);
#35418=PRESENTATION_STYLE_ASSIGNMENT((#35417));
ENDSEC;
END-ISO-10303-21;
